ISO-10303-21;
HEADER;
/* Generated by software containing ST-Developer
 * from STEP Tools, Inc. (www.steptools.com) 
 */

FILE_DESCRIPTION(
/* description */ ('Indexing fixture plate with plunger'),
/* implementation_level */ '2;1');

FILE_NAME(
/* name */ 'Bonded foot (2).step',
/* time_stamp */ '2026-10-28T03:23:41-07:00',
/* author */ (''),
/* organization */ (''),
/* preprocessor_version */ 'ST-DEVELOPER v20.2',
/* originating_system */ 'Autodesk Translation Framework v15.17.0.0',
/* authorisation */ '');

FILE_SCHEMA (('AUTOMOTIVE_DESIGN { 1 0 10303 214 3 1 1 }'));
ENDSEC;

DATA;
#10=MECHANICAL_DESIGN_GEOMETRIC_PRESENTATION_REPRESENTATION('',(#320),#10020);
#266=SHAPE_REPRESENTATION_RELATIONSHIP('SRR','None',#10140,#293);
#293=ADVANCED_BREP_SHAPE_REPRESENTATION('',(#356),#9993);
#320=STYLED_ITEM('',(#10382),#356);
#356=MANIFOLD_SOLID_BREP('Body1',#4574);
#547=PLANE('',#4953);
#548=PLANE('',#4954);
#689=FACE_OUTER_BOUND('',#989,.T.);
#690=FACE_OUTER_BOUND('',#990,.T.);
#691=FACE_OUTER_BOUND('',#991,.T.);
#989=EDGE_LOOP('',(#3141,#3142,#3143,#3144));
#990=EDGE_LOOP('',(#3145));
#991=EDGE_LOOP('',(#3146));
#1413=LINE('',#7219,#1633);
#1633=VECTOR('',#5684,1.);
#1850=CIRCLE('',#4951,1.);
#1851=CIRCLE('',#4952,1.);
#2161=VERTEX_POINT('',#7216);
#2162=VERTEX_POINT('',#7218);
#2550=EDGE_CURVE('',#2161,#2161,#1850,.T.);
#2551=EDGE_CURVE('',#2161,#2162,#1413,.T.);
#2552=EDGE_CURVE('',#2162,#2162,#1851,.T.);
#3141=ORIENTED_EDGE('',*,*,#2550,.F.);
#3142=ORIENTED_EDGE('',*,*,#2551,.T.);
#3143=ORIENTED_EDGE('',*,*,#2552,.T.);
#3144=ORIENTED_EDGE('',*,*,#2551,.F.);
#3145=ORIENTED_EDGE('',*,*,#2550,.T.);
#3146=ORIENTED_EDGE('',*,*,#2552,.F.);
#4176=CYLINDRICAL_SURFACE('',#4950,1.);
#4304=ADVANCED_FACE('',(#689),#4176,.T.);
#4305=ADVANCED_FACE('',(#690),#547,.T.);
#4306=ADVANCED_FACE('',(#691),#548,.F.);
#4574=CLOSED_SHELL('',(#4304,#4305,#4306));
#4949=AXIS2_PLACEMENT_3D('',#7214,#5678,#5679);
#4950=AXIS2_PLACEMENT_3D('',#7215,#5680,#5681);
#4951=AXIS2_PLACEMENT_3D('',#7217,#5682,#5683);
#4952=AXIS2_PLACEMENT_3D('',#7220,#5685,#5686);
#4953=AXIS2_PLACEMENT_3D('',#7221,#5687,#5688);
#4954=AXIS2_PLACEMENT_3D('',#7222,#5689,#5690);
#5678=DIRECTION('axis',(0.,0.,1.));
#5679=DIRECTION('refdir',(1.,0.,0.));
#5680=DIRECTION('center_axis',(0.,0.,1.));
#5681=DIRECTION('ref_axis',(1.,0.,0.));
#5682=DIRECTION('center_axis',(0.,0.,1.));
#5683=DIRECTION('ref_axis',(1.,0.,0.));
#5684=DIRECTION('',(0.,0.,-1.));
#5685=DIRECTION('center_axis',(0.,0.,1.));
#5686=DIRECTION('ref_axis',(1.,0.,0.));
#5687=DIRECTION('center_axis',(0.,0.,1.));
#5688=DIRECTION('ref_axis',(1.,0.,0.));
#5689=DIRECTION('center_axis',(0.,0.,1.));
#5690=DIRECTION('ref_axis',(1.,0.,0.));
#7214=CARTESIAN_POINT('',(0.,0.,0.));
#7215=CARTESIAN_POINT('Origin',(9.5,-9.5,-3.5));
#7216=CARTESIAN_POINT('',(8.5,-9.5,-1.));
#7217=CARTESIAN_POINT('Origin',(9.5,-9.5,-1.));
#7218=CARTESIAN_POINT('',(8.5,-9.5,-3.5));
#7219=CARTESIAN_POINT('',(8.5,-9.5,-3.5));
#7220=CARTESIAN_POINT('Origin',(9.5,-9.5,-3.5));
#7221=CARTESIAN_POINT('Origin',(9.5,-9.5,-1.));
#7222=CARTESIAN_POINT('Origin',(9.5,-9.5,-3.5));
#9960=UNCERTAINTY_MEASURE_WITH_UNIT(LENGTH_MEASURE(0.001),#10021,
'DISTANCE_ACCURACY_VALUE',
'Maximum model space distance between geometric entities at asserted c
onnectivities');
#9987=UNCERTAINTY_MEASURE_WITH_UNIT(LENGTH_MEASURE(0.001),#10021,
'DISTANCE_ACCURACY_VALUE',
'Maximum model space distance between geometric entities at asserted c
onnectivities');
#9993=(
GEOMETRIC_REPRESENTATION_CONTEXT(3)
GLOBAL_UNCERTAINTY_ASSIGNED_CONTEXT((#9960))
GLOBAL_UNIT_ASSIGNED_CONTEXT((#10021,#10023,#10024))
REPRESENTATION_CONTEXT('','3D')
);
#10020=(
GEOMETRIC_REPRESENTATION_CONTEXT(3)
GLOBAL_UNCERTAINTY_ASSIGNED_CONTEXT((#9987))
GLOBAL_UNIT_ASSIGNED_CONTEXT((#10021,#10023,#10024))
REPRESENTATION_CONTEXT('','3D')
);
#10021=(
LENGTH_UNIT()
NAMED_UNIT(*)
SI_UNIT(.CENTI.,.METRE.)
);
#10023=(
NAMED_UNIT(*)
PLANE_ANGLE_UNIT()
SI_UNIT($,.RADIAN.)
);
#10024=(
NAMED_UNIT(*)
SI_UNIT($,.STERADIAN.)
SOLID_ANGLE_UNIT()
);
#10030=SHAPE_DEFINITION_REPRESENTATION(#10062,#10140);
#10062=PRODUCT_DEFINITION_SHAPE('',$,#10173);
#10140=SHAPE_REPRESENTATION('',(#4949),#9993);
#10167=PRODUCT_DEFINITION_CONTEXT('part definition',#10265,'design');
#10173=PRODUCT_DEFINITION('Bonded foot (2)','Bonded foot (2)',#10205,#10167);
#10205=PRODUCT_DEFINITION_FORMATION('',$,#10272);
#10265=APPLICATION_CONTEXT(
'Core Data for Automotive Mechanical Design Process');
#10266=PRODUCT_CONTEXT('part definition',#10265,'mechanical');
#10272=PRODUCT('Bonded foot (2)','Bonded foot (2)','Bonded foot (2)',(#10266));
#10376=COLOUR_RGB('Off White',0.89,0.88,0.83);
#10377=FILL_AREA_STYLE_COLOUR('',#10376);
#10378=FILL_AREA_STYLE('',(#10377));
#10379=SURFACE_STYLE_FILL_AREA(#10378);
#10380=SURFACE_SIDE_STYLE('',(#10379));
#10381=SURFACE_STYLE_USAGE(.BOTH.,#10380);
#10382=PRESENTATION_STYLE_ASSIGNMENT((#10381));
ENDSEC;
END-ISO-10303-21;
